ISO-10303-21;
HEADER;
/* Generated by software containing ST-Developer
 * from STEP Tools, Inc. (www.steptools.com) 
 */

FILE_DESCRIPTION(
/* description */ ('Shaft runout checking stand'),
/* implementation_level */ '2;1');

FILE_NAME(
/* name */ 'Socket Set Screw - M5x8.step',
/* time_stamp */ '2026-11-02T21:12:33-08:00',
/* author */ (''),
/* organization */ (''),
/* preprocessor_version */ 'ST-DEVELOPER v20.2',
/* originating_system */ 'Autodesk Translation Framework v15.17.0.0',
/* authorisation */ '');

FILE_SCHEMA (('AUTOMOTIVE_DESIGN { 1 0 10303 214 3 1 1 }'));
ENDSEC;

DATA;
#10=MECHANICAL_DESIGN_GEOMETRIC_PRESENTATION_REPRESENTATION('',(#489),#11748);
#369=CONICAL_SURFACE('',#7188,0.235,0.785398163397448);
#370=CONICAL_SURFACE('',#7192,0.2125,0.785398163397448);
#403=SHAPE_REPRESENTATION_RELATIONSHIP('SRR','None',#11952,#446);
#446=ADVANCED_BREP_SHAPE_REPRESENTATION('',(#537),#11728);
#489=STYLED_ITEM('',(#12172),#537);
#537=MANIFOLD_SOLID_BREP('Body1',#6235);
#649=FACE_BOUND('',#1761,.T.);
#827=CIRCLE('',#7187,0.22);
#828=CIRCLE('',#7189,0.24505);
#829=CIRCLE('',#7191,0.24505);
#830=CIRCLE('',#7193,0.175);
#1007=CYLINDRICAL_SURFACE('',#7190,0.24505);
#1298=FACE_OUTER_BOUND('',#1753,.T.);
#1299=FACE_OUTER_BOUND('',#1754,.T.);
#1300=FACE_OUTER_BOUND('',#1755,.T.);
#1301=FACE_OUTER_BOUND('',#1756,.T.);
#1302=FACE_OUTER_BOUND('',#1757,.T.);
#1303=FACE_OUTER_BOUND('',#1758,.T.);
#1304=FACE_OUTER_BOUND('',#1759,.T.);
#1305=FACE_OUTER_BOUND('',#1760,.T.);
#1306=FACE_OUTER_BOUND('',#1762,.T.);
#1307=FACE_OUTER_BOUND('',#1763,.T.);
#1308=FACE_OUTER_BOUND('',#1764,.T.);
#1309=FACE_OUTER_BOUND('',#1765,.T.);
#1753=EDGE_LOOP('',(#5214,#5215,#5216,#5217));
#1754=EDGE_LOOP('',(#5218,#5219,#5220,#5221));
#1755=EDGE_LOOP('',(#5222,#5223,#5224,#5225));
#1756=EDGE_LOOP('',(#5226,#5227,#5228,#5229));
#1757=EDGE_LOOP('',(#5230,#5231,#5232,#5233));
#1758=EDGE_LOOP('',(#5234,#5235,#5236,#5237));
#1759=EDGE_LOOP('',(#5238,#5239,#5240,#5241,#5242,#5243));
#1760=EDGE_LOOP('',(#5244));
#1761=EDGE_LOOP('',(#5245,#5246,#5247,#5248,#5249,#5250));
#1762=EDGE_LOOP('',(#5251,#5252,#5253,#5254));
#1763=EDGE_LOOP('',(#5255,#5256,#5257,#5258));
#1764=EDGE_LOOP('',(#5259,#5260,#5261,#5262));
#1765=EDGE_LOOP('',(#5263));
#2288=LINE('',#10746,#2755);
#2289=LINE('',#10748,#2756);
#2290=LINE('',#10750,#2757);
#2291=LINE('',#10751,#2758);
#2292=LINE('',#10754,#2759);
#2293=LINE('',#10756,#2760);
#2294=LINE('',#10757,#2761);
#2295=LINE('',#10760,#2762);
#2296=LINE('',#10762,#2763);
#2297=LINE('',#10763,#2764);
#2298=LINE('',#10766,#2765);
#2299=LINE('',#10768,#2766);
#2300=LINE('',#10769,#2767);
#2301=LINE('',#10772,#2768);
#2302=LINE('',#10774,#2769);
#2303=LINE('',#10775,#2770);
#2304=LINE('',#10777,#2771);
#2305=LINE('',#10778,#2772);
#2306=LINE('',#10786,#2773);
#2307=LINE('',#10790,#2774);
#2308=LINE('',#10794,#2775);
#2755=VECTOR('',#8787,1.);
#2756=VECTOR('',#8788,1.);
#2757=VECTOR('',#8789,1.);
#2758=VECTOR('',#8790,1.);
#2759=VECTOR('',#8793,1.);
#2760=VECTOR('',#8794,1.);
#2761=VECTOR('',#8795,1.);
#2762=VECTOR('',#8798,1.);
#2763=VECTOR('',#8799,1.);
#2764=VECTOR('',#8800,1.);
#2765=VECTOR('',#8803,1.);
#2766=VECTOR('',#8804,1.);
#2767=VECTOR('',#8805,1.);
#2768=VECTOR('',#8808,1.);
#2769=VECTOR('',#8809,1.);
#2770=VECTOR('',#8810,1.);
#2771=VECTOR('',#8813,1.);
#2772=VECTOR('',#8814,1.);
#2773=VECTOR('',#8825,0.235);
#2774=VECTOR('',#8830,0.25);
#2775=VECTOR('',#8835,0.2125);
#3191=VERTEX_POINT('',#10744);
#3192=VERTEX_POINT('',#10745);
#3193=VERTEX_POINT('',#10747);
#3194=VERTEX_POINT('',#10749);
#3195=VERTEX_POINT('',#10753);
#3196=VERTEX_POINT('',#10755);
#3197=VERTEX_POINT('',#10759);
#3198=VERTEX_POINT('',#10761);
#3199=VERTEX_POINT('',#10765);
#3200=VERTEX_POINT('',#10767);
#3201=VERTEX_POINT('',#10771);
#3202=VERTEX_POINT('',#10773);
#3203=VERTEX_POINT('',#10781);
#3204=VERTEX_POINT('',#10784);
#3205=VERTEX_POINT('',#10788);
#3206=VERTEX_POINT('',#10792);
#3893=EDGE_CURVE('',#3191,#3192,#2288,.T.);
#3894=EDGE_CURVE('',#3191,#3193,#2289,.T.);
#3895=EDGE_CURVE('',#3193,#3194,#2290,.T.);
#3896=EDGE_CURVE('',#3192,#3194,#2291,.T.);
#3897=EDGE_CURVE('',#3195,#3191,#2292,.T.);
#3898=EDGE_CURVE('',#3195,#3196,#2293,.T.);
#3899=EDGE_CURVE('',#3196,#3193,#2294,.T.);
#3900=EDGE_CURVE('',#3197,#3195,#2295,.T.);
#3901=EDGE_CURVE('',#3197,#3198,#2296,.T.);
#3902=EDGE_CURVE('',#3198,#3196,#2297,.T.);
#3903=EDGE_CURVE('',#3199,#3197,#2298,.T.);
#3904=EDGE_CURVE('',#3199,#3200,#2299,.T.);
#3905=EDGE_CURVE('',#3200,#3198,#2300,.T.);
#3906=EDGE_CURVE('',#3201,#3199,#2301,.T.);
#3907=EDGE_CURVE('',#3201,#3202,#2302,.T.);
#3908=EDGE_CURVE('',#3202,#3200,#2303,.T.);
#3909=EDGE_CURVE('',#3192,#3201,#2304,.T.);
#3910=EDGE_CURVE('',#3194,#3202,#2305,.T.);
#3911=EDGE_CURVE('',#3203,#3203,#827,.T.);
#3912=EDGE_CURVE('',#3204,#3204,#828,.T.);
#3913=EDGE_CURVE('',#3204,#3203,#2306,.T.);
#3914=EDGE_CURVE('',#3205,#3205,#829,.F.);
#3915=EDGE_CURVE('',#3205,#3204,#2307,.T.);
#3916=EDGE_CURVE('',#3206,#3206,#830,.T.);
#3917=EDGE_CURVE('',#3206,#3205,#2308,.T.);
#5214=ORIENTED_EDGE('',*,*,#3893,.F.);
#5215=ORIENTED_EDGE('',*,*,#3894,.T.);
#5216=ORIENTED_EDGE('',*,*,#3895,.T.);
#5217=ORIENTED_EDGE('',*,*,#3896,.F.);
#5218=ORIENTED_EDGE('',*,*,#3897,.F.);
#5219=ORIENTED_EDGE('',*,*,#3898,.T.);
#5220=ORIENTED_EDGE('',*,*,#3899,.T.);
#5221=ORIENTED_EDGE('',*,*,#3894,.F.);
#5222=ORIENTED_EDGE('',*,*,#3900,.F.);
#5223=ORIENTED_EDGE('',*,*,#3901,.T.);
#5224=ORIENTED_EDGE('',*,*,#3902,.T.);
#5225=ORIENTED_EDGE('',*,*,#3898,.F.);
#5226=ORIENTED_EDGE('',*,*,#3903,.F.);
#5227=ORIENTED_EDGE('',*,*,#3904,.T.);
#5228=ORIENTED_EDGE('',*,*,#3905,.T.);
#5229=ORIENTED_EDGE('',*,*,#3901,.F.);
#5230=ORIENTED_EDGE('',*,*,#3906,.F.);
#5231=ORIENTED_EDGE('',*,*,#3907,.T.);
#5232=ORIENTED_EDGE('',*,*,#3908,.T.);
#5233=ORIENTED_EDGE('',*,*,#3904,.F.);
#5234=ORIENTED_EDGE('',*,*,#3909,.F.);
#5235=ORIENTED_EDGE('',*,*,#3896,.T.);
#5236=ORIENTED_EDGE('',*,*,#3910,.T.);
#5237=ORIENTED_EDGE('',*,*,#3907,.F.);
#5238=ORIENTED_EDGE('',*,*,#3910,.F.);
#5239=ORIENTED_EDGE('',*,*,#3895,.F.);
#5240=ORIENTED_EDGE('',*,*,#3899,.F.);
#5241=ORIENTED_EDGE('',*,*,#3902,.F.);
#5242=ORIENTED_EDGE('',*,*,#3905,.F.);
#5243=ORIENTED_EDGE('',*,*,#3908,.F.);
#5244=ORIENTED_EDGE('',*,*,#3911,.F.);
#5245=ORIENTED_EDGE('',*,*,#3893,.T.);
#5246=ORIENTED_EDGE('',*,*,#3909,.T.);
#5247=ORIENTED_EDGE('',*,*,#3906,.T.);
#5248=ORIENTED_EDGE('',*,*,#3903,.T.);
#5249=ORIENTED_EDGE('',*,*,#3900,.T.);
#5250=ORIENTED_EDGE('',*,*,#3897,.T.);
#5251=ORIENTED_EDGE('',*,*,#3912,.F.);
#5252=ORIENTED_EDGE('',*,*,#3913,.T.);
#5253=ORIENTED_EDGE('',*,*,#3911,.T.);
#5254=ORIENTED_EDGE('',*,*,#3913,.F.);
#5255=ORIENTED_EDGE('',*,*,#3914,.F.);
#5256=ORIENTED_EDGE('',*,*,#3915,.T.);
#5257=ORIENTED_EDGE('',*,*,#3912,.T.);
#5258=ORIENTED_EDGE('',*,*,#3915,.F.);
#5259=ORIENTED_EDGE('',*,*,#3916,.F.);
#5260=ORIENTED_EDGE('',*,*,#3917,.T.);
#5261=ORIENTED_EDGE('',*,*,#3914,.T.);
#5262=ORIENTED_EDGE('',*,*,#3917,.F.);
#5263=ORIENTED_EDGE('',*,*,#3916,.T.);
#5785=PLANE('',#7179);
#5786=PLANE('',#7180);
#5787=PLANE('',#7181);
#5788=PLANE('',#7182);
#5789=PLANE('',#7183);
#5790=PLANE('',#7184);
#5791=PLANE('',#7185);
#5792=PLANE('',#7186);
#5793=PLANE('',#7194);
#6098=ADVANCED_FACE('',(#1298),#5785,.F.);
#6099=ADVANCED_FACE('',(#1299),#5786,.F.);
#6100=ADVANCED_FACE('',(#1300),#5787,.F.);
#6101=ADVANCED_FACE('',(#1301),#5788,.F.);
#6102=ADVANCED_FACE('',(#1302),#5789,.F.);
#6103=ADVANCED_FACE('',(#1303),#5790,.F.);
#6104=ADVANCED_FACE('',(#1304),#5791,.F.);
#6105=ADVANCED_FACE('',(#1305,#649),#5792,.T.);
#6106=ADVANCED_FACE('',(#1306),#369,.T.);
#6107=ADVANCED_FACE('',(#1307),#1007,.T.);
#6108=ADVANCED_FACE('',(#1308),#370,.T.);
#6109=ADVANCED_FACE('',(#1309),#5793,.T.);
#6235=CLOSED_SHELL('',(#6098,#6099,#6100,#6101,#6102,#6103,#6104,#6105,
#6106,#6107,#6108,#6109));
#7178=AXIS2_PLACEMENT_3D('',#10742,#8783,#8784);
#7179=AXIS2_PLACEMENT_3D('',#10743,#8785,#8786);
#7180=AXIS2_PLACEMENT_3D('',#10752,#8791,#8792);
#7181=AXIS2_PLACEMENT_3D('',#10758,#8796,#8797);
#7182=AXIS2_PLACEMENT_3D('',#10764,#8801,#8802);
#7183=AXIS2_PLACEMENT_3D('',#10770,#8806,#8807);
#7184=AXIS2_PLACEMENT_3D('',#10776,#8811,#8812);
#7185=AXIS2_PLACEMENT_3D('',#10779,#8815,#8816);
#7186=AXIS2_PLACEMENT_3D('',#10780,#8817,#8818);
#7187=AXIS2_PLACEMENT_3D('',#10782,#8819,#8820);
#7188=AXIS2_PLACEMENT_3D('',#10783,#8821,#8822);
#7189=AXIS2_PLACEMENT_3D('',#10785,#8823,#8824);
#7190=AXIS2_PLACEMENT_3D('',#10787,#8826,#8827);
#7191=AXIS2_PLACEMENT_3D('',#10789,#8828,#8829);
#7192=AXIS2_PLACEMENT_3D('',#10791,#8831,#8832);
#7193=AXIS2_PLACEMENT_3D('',#10793,#8833,#8834);
#7194=AXIS2_PLACEMENT_3D('',#10795,#8836,#8837);
#8783=DIRECTION('axis',(0.,0.,1.));
#8784=DIRECTION('refdir',(1.,0.,0.));
#8785=DIRECTION('center_axis',(0.866025403784439,0.,-0.5));
#8786=DIRECTION('ref_axis',(0.5,0.,0.866025403784439));
#8787=DIRECTION('',(0.5,0.,0.866025403784439));
#8788=DIRECTION('',(0.,-1.,0.));
#8789=DIRECTION('',(0.5,0.,0.866025403784439));
#8790=DIRECTION('',(0.,-1.,0.));
#8791=DIRECTION('center_axis',(1.92296268638356E-16,0.,-1.));
#8792=DIRECTION('ref_axis',(1.,0.,1.92296268638356E-16));
#8793=DIRECTION('',(1.,0.,1.92296268638356E-16));
#8794=DIRECTION('',(0.,-1.,0.));
#8795=DIRECTION('',(1.,0.,1.92296268638356E-16));
#8796=DIRECTION('center_axis',(-0.866025403784439,0.,-0.5));
#8797=DIRECTION('ref_axis',(0.5,0.,-0.866025403784439));
#8798=DIRECTION('',(0.5,0.,-0.866025403784439));
#8799=DIRECTION('',(0.,-1.,0.));
#8800=DIRECTION('',(0.5,0.,-0.866025403784438));
#8801=DIRECTION('center_axis',(-0.866025403784439,0.,0.5));
#8802=DIRECTION('ref_axis',(-0.5,0.,-0.866025403784439));
#8803=DIRECTION('',(-0.5,0.,-0.866025403784439));
#8804=DIRECTION('',(0.,-1.,0.));
#8805=DIRECTION('',(-0.5,0.,-0.866025403784439));
#8806=DIRECTION('center_axis',(-1.92296268638356E-16,0.,1.));
#8807=DIRECTION('ref_axis',(-1.,0.,-1.92296268638356E-16));
#8808=DIRECTION('',(-1.,0.,-1.92296268638356E-16));
#8809=DIRECTION('',(0.,-1.,0.));
#8810=DIRECTION('',(-1.,0.,-1.92296268638356E-16));
#8811=DIRECTION('center_axis',(0.866025403784439,0.,0.5));
#8812=DIRECTION('ref_axis',(-0.5,0.,0.866025403784439));
#8813=DIRECTION('',(-0.5,0.,0.866025403784439));
#8814=DIRECTION('',(-0.5,0.,0.866025403784439));
#8815=DIRECTION('center_axis',(0.,-1.,0.));
#8816=DIRECTION('ref_axis',(0.,0.,-1.));
#8817=DIRECTION('center_axis',(0.,1.,0.));
#8818=DIRECTION('ref_axis',(0.,0.,1.));
#8819=DIRECTION('center_axis',(0.,-1.,0.));
#8820=DIRECTION('ref_axis',(1.,0.,0.));
#8821=DIRECTION('center_axis',(0.,-1.,0.));
#8822=DIRECTION('ref_axis',(1.,0.,0.));
#8823=DIRECTION('center_axis',(0.,-1.,0.));
#8824=DIRECTION('ref_axis',(1.,0.,0.));
#8825=DIRECTION('',(0.707106781186547,0.707106781186548,8.65956056235493E-17));
#8826=DIRECTION('center_axis',(0.,-1.,0.));
#8827=DIRECTION('ref_axis',(1.,0.,0.));
#8828=DIRECTION('center_axis',(0.,1.,0.));
#8829=DIRECTION('ref_axis',(1.,0.,0.));
#8830=DIRECTION('',(0.,1.,0.));
#8831=DIRECTION('center_axis',(0.,1.,0.));
#8832=DIRECTION('ref_axis',(1.,0.,0.));
#8833=DIRECTION('center_axis',(0.,-1.,0.));
#8834=DIRECTION('ref_axis',(1.,0.,0.));
#8835=DIRECTION('',(-0.707106781186547,0.707106781186548,-8.65956056235493E-17));
#8836=DIRECTION('center_axis',(0.,-1.,0.));
#8837=DIRECTION('ref_axis',(0.,0.,-1.));
#10742=CARTESIAN_POINT('',(0.,0.,0.));
#10743=CARTESIAN_POINT('Origin',(0.0721687836487032,0.,-0.125));
#10744=CARTESIAN_POINT('',(0.0721687836487032,0.,-0.125));
#10745=CARTESIAN_POINT('',(0.144337567297406,0.,0.));
#10746=CARTESIAN_POINT('',(0.117710979560879,0.,-0.0461186027918559));
#10747=CARTESIAN_POINT('',(0.0721687836487032,-0.25,-0.125));
#10748=CARTESIAN_POINT('',(0.0721687836487032,0.,-0.125));
#10749=CARTESIAN_POINT('',(0.144337567297406,-0.25,0.));
#10750=CARTESIAN_POINT('',(0.144337567297406,-0.25,0.));
#10751=CARTESIAN_POINT('',(0.144337567297406,0.,0.));
#10752=CARTESIAN_POINT('Origin',(-0.0721687836487032,0.,-0.125));
#10753=CARTESIAN_POINT('',(-0.0721687836487032,0.,-0.125));
#10754=CARTESIAN_POINT('',(0.0739156081756484,0.,-0.125));
#10755=CARTESIAN_POINT('',(-0.0721687836487032,-0.25,-0.125));
#10756=CARTESIAN_POINT('',(-0.0721687836487032,0.,-0.125));
#10757=CARTESIAN_POINT('',(0.0721687836487032,-0.25,-0.125));
#10758=CARTESIAN_POINT('Origin',(-0.144337567297406,0.,-4.16333634234434E-17));
#10759=CARTESIAN_POINT('',(-0.144337567297406,0.,-1.76762539787485E-17));
#10760=CARTESIAN_POINT('',(-0.0987953713852306,0.,-0.0788813972081442));
#10761=CARTESIAN_POINT('',(-0.144337567297406,-0.25,-2.77555756156289E-17));
#10762=CARTESIAN_POINT('',(-0.144337567297406,0.,-1.76762539787485E-17));
#10763=CARTESIAN_POINT('',(-0.0721687836487032,-0.25,-0.125));
#10764=CARTESIAN_POINT('Origin',(-0.0721687836487033,0.,0.125));
#10765=CARTESIAN_POINT('',(-0.0721687836487033,0.,0.125));
#10766=CARTESIAN_POINT('',(-0.0627109795608791,0.,0.141381397208144));
#10767=CARTESIAN_POINT('',(-0.0721687836487033,-0.25,0.125));
#10768=CARTESIAN_POINT('',(-0.0721687836487033,0.,0.125));
#10769=CARTESIAN_POINT('',(-0.144337567297406,-0.25,-1.76762539787485E-17));
#10770=CARTESIAN_POINT('Origin',(0.0721687836487032,0.,0.125));
#10771=CARTESIAN_POINT('',(0.0721687836487032,0.,0.125));
#10772=CARTESIAN_POINT('',(0.146084391824352,0.,0.125));
#10773=CARTESIAN_POINT('',(0.0721687836487032,-0.25,0.125));
#10774=CARTESIAN_POINT('',(0.0721687836487032,0.,0.125));
#10775=CARTESIAN_POINT('',(-0.0721687836487033,-0.25,0.125));
#10776=CARTESIAN_POINT('Origin',(0.144337567297406,0.,0.));
#10777=CARTESIAN_POINT('',(0.153795371385231,0.,-0.0163813972081441));
#10778=CARTESIAN_POINT('',(0.0721687836487032,-0.25,0.125));
#10779=CARTESIAN_POINT('Origin',(0.,-0.25,0.));
#10780=CARTESIAN_POINT('Origin',(0.22,0.,0.));
#10781=CARTESIAN_POINT('',(-0.22,-8.67361737988404E-18,-2.69422295812418E-17));
#10782=CARTESIAN_POINT('Origin',(0.,0.,0.));
#10783=CARTESIAN_POINT('Origin',(0.,-0.015,0.));
#10784=CARTESIAN_POINT('',(-0.24505,-0.02505,-3.00099698131059E-17));
#10785=CARTESIAN_POINT('Origin',(0.,-0.02505,0.));
#10786=CARTESIAN_POINT('',(-0.235,-0.015,-2.87791997799628E-17));
#10787=CARTESIAN_POINT('Origin',(0.,-0.3775,0.));
#10788=CARTESIAN_POINT('',(-0.24505,-0.72995,3.00099698131059E-17));
#10789=CARTESIAN_POINT('Origin',(0.,-0.72995,0.));
#10790=CARTESIAN_POINT('',(-0.24505,-0.3775,-3.00099698131059E-17));
#10791=CARTESIAN_POINT('Origin',(0.,-0.7625,0.));
#10792=CARTESIAN_POINT('',(-0.175,-0.8,-2.14313189850787E-17));
#10793=CARTESIAN_POINT('Origin',(0.,-0.8,0.));
#10794=CARTESIAN_POINT('',(-0.2125,-0.7625,-2.60237444818813E-17));
#10795=CARTESIAN_POINT('Origin',(0.,-0.8,0.));
#11679=UNCERTAINTY_MEASURE_WITH_UNIT(LENGTH_MEASURE(0.001),#11749,
'DISTANCE_ACCURACY_VALUE',
'Maximum model space distance between geometric entities at asserted c
onnectivities');
#11699=UNCERTAINTY_MEASURE_WITH_UNIT(LENGTH_MEASURE(0.001),#11749,
'DISTANCE_ACCURACY_VALUE',
'Maximum model space distance between geometric entities at asserted c
onnectivities');
#11728=(
GEOMETRIC_REPRESENTATION_CONTEXT(3)
GLOBAL_UNCERTAINTY_ASSIGNED_CONTEXT((#11679))
GLOBAL_UNIT_ASSIGNED_CONTEXT((#11749,#11751,#11752))
REPRESENTATION_CONTEXT('','3D')
);
#11748=(
GEOMETRIC_REPRESENTATION_CONTEXT(3)
GLOBAL_UNCERTAINTY_ASSIGNED_CONTEXT((#11699))
GLOBAL_UNIT_ASSIGNED_CONTEXT((#11749,#11751,#11752))
REPRESENTATION_CONTEXT('','3D')
);
#11749=(
LENGTH_UNIT()
NAMED_UNIT(*)
SI_UNIT(.CENTI.,.METRE.)
);
#11751=(
NAMED_UNIT(*)
PLANE_ANGLE_UNIT()
SI_UNIT($,.RADIAN.)
);
#11752=(
NAMED_UNIT(*)
SI_UNIT($,.STERADIAN.)
SOLID_ANGLE_UNIT()
);
#11781=SHAPE_DEFINITION_REPRESENTATION(#11829,#11952);
#11829=PRODUCT_DEFINITION_SHAPE('',$,#12001);
#11952=SHAPE_REPRESENTATION('',(#7178),#11728);
#11972=PRODUCT_DEFINITION_CONTEXT('part definition',#12118,'design');
#12001=PRODUCT_DEFINITION('Socket Set Screw - M5x8',
'Socket Set Screw - M5x8',#12049,#11972);
#12049=PRODUCT_DEFINITION_FORMATION('',$,#12148);
#12118=APPLICATION_CONTEXT(
'Core Data for Automotive Mechanical Design Process');
#12119=PRODUCT_CONTEXT('part definition',#12118,'mechanical');
#12148=PRODUCT('Socket Set Screw - M5x8','Socket Set Screw - M5x8',
'Socket Set Screw - M5x8',(#12119));
#12172=PRESENTATION_STYLE_ASSIGNMENT((#12177));
#12177=SURFACE_STYLE_USAGE(.BOTH.,#12182);
#12182=SURFACE_SIDE_STYLE('',(#12187));
#12187=SURFACE_STYLE_FILL_AREA(#12192);
#12192=FILL_AREA_STYLE('CAD Library Painted - Graphite',(#12197));
#12197=FILL_AREA_STYLE_COLOUR('CAD Library Painted - Graphite',#12202);
#12202=COLOUR_RGB('CAD Library Painted - Graphite',0.168627450980392,0.192156862745098,
0.231372549019608);
ENDSEC;
END-ISO-10303-21;
